ISO-10303-21;
HEADER;
/* Generated by software containing ST-Developer
 * from STEP Tools, Inc. (www.steptools.com) 
 */

FILE_DESCRIPTION(
/* description */ ('Round-Shaft Linear Stage with Ball Bushings'),
/* implementation_level */ '2;1');

FILE_NAME(
/* name */ 'Cap Screw - M4x16.step',
/* time_stamp */ '2026-10-27T10:47:55-07:00',
/* author */ (''),
/* organization */ (''),
/* preprocessor_version */ 'ST-DEVELOPER v20.2',
/* originating_system */ 'Autodesk Translation Framework v15.17.0.0',
/* authorisation */ '');

FILE_SCHEMA (('AUTOMOTIVE_DESIGN { 1 0 10303 214 3 1 1 }'));
ENDSEC;

DATA;
#10=MECHANICAL_DESIGN_GEOMETRIC_PRESENTATION_REPRESENTATION('',(#319),#7835);
#236=ORIENTED_CLOSED_SHELL('',*,#4411,.F.);
#240=BREP_WITH_VOIDS('Body1',#4410,(#236));
#248=CONICAL_SURFACE('',#5038,0.325,0.785398163397448);
#249=CONICAL_SURFACE('',#5042,0.335,0.785398163397448);
#250=CONICAL_SURFACE('',#5046,0.21,0.463647609000806);
#251=CONICAL_SURFACE('',#5050,0.18,0.785398163397448);
#277=SHAPE_REPRESENTATION_RELATIONSHIP('SRR','None',#7967,#298);
#298=ADVANCED_BREP_SHAPE_REPRESENTATION('',(#240),#7831);
#319=STYLED_ITEM('',(#8151),#240);
#454=FACE_BOUND('',#1194,.T.);
#581=PLANE('',#5036);
#582=PLANE('',#5044);
#583=PLANE('',#5052);
#584=PLANE('',#5053);
#585=PLANE('',#5054);
#586=PLANE('',#5055);
#587=PLANE('',#5056);
#588=PLANE('',#5057);
#589=PLANE('',#5058);
#590=PLANE('',#5059);
#591=PLANE('',#5060);
#818=FACE_OUTER_BOUND('',#1189,.T.);
#819=FACE_OUTER_BOUND('',#1190,.T.);
#820=FACE_OUTER_BOUND('',#1191,.T.);
#821=FACE_OUTER_BOUND('',#1192,.T.);
#822=FACE_OUTER_BOUND('',#1193,.T.);
#823=FACE_OUTER_BOUND('',#1195,.T.);
#824=FACE_OUTER_BOUND('',#1196,.T.);
#825=FACE_OUTER_BOUND('',#1197,.T.);
#826=FACE_OUTER_BOUND('',#1198,.T.);
#827=FACE_OUTER_BOUND('',#1199,.T.);
#828=FACE_OUTER_BOUND('',#1200,.T.);
#829=FACE_OUTER_BOUND('',#1201,.T.);
#830=FACE_OUTER_BOUND('',#1202,.T.);
#831=FACE_OUTER_BOUND('',#1203,.T.);
#832=FACE_OUTER_BOUND('',#1204,.T.);
#833=FACE_OUTER_BOUND('',#1205,.T.);
#834=FACE_OUTER_BOUND('',#1206,.T.);
#1189=EDGE_LOOP('',(#3848));
#1190=EDGE_LOOP('',(#3849,#3850,#3851,#3852));
#1191=EDGE_LOOP('',(#3853,#3854,#3855,#3856));
#1192=EDGE_LOOP('',(#3857,#3858,#3859,#3860));
#1193=EDGE_LOOP('',(#3861));
#1194=EDGE_LOOP('',(#3862));
#1195=EDGE_LOOP('',(#3863,#3864,#3865,#3866));
#1196=EDGE_LOOP('',(#3867,#3868,#3869,#3870));
#1197=EDGE_LOOP('',(#3871,#3872,#3873,#3874));
#1198=EDGE_LOOP('',(#3875));
#1199=EDGE_LOOP('',(#3876,#3877,#3878,#3879));
#1200=EDGE_LOOP('',(#3880,#3881,#3882,#3883));
#1201=EDGE_LOOP('',(#3884,#3885,#3886,#3887));
#1202=EDGE_LOOP('',(#3888,#3889,#3890,#3891));
#1203=EDGE_LOOP('',(#3892,#3893,#3894,#3895));
#1204=EDGE_LOOP('',(#3896,#3897,#3898,#3899));
#1205=EDGE_LOOP('',(#3900,#3901,#3902,#3903,#3904,#3905));
#1206=EDGE_LOOP('',(#3906,#3907,#3908,#3909,#3910,#3911));
#1515=LINE('',#7512,#1855);
#1516=LINE('',#7516,#1856);
#1517=LINE('',#7520,#1857);
#1518=LINE('',#7527,#1858);
#1519=LINE('',#7531,#1859);
#1520=LINE('',#7535,#1860);
#1521=LINE('',#7540,#1861);
#1522=LINE('',#7542,#1862);
#1523=LINE('',#7544,#1863);
#1524=LINE('',#7545,#1864);
#1525=LINE('',#7548,#1865);
#1526=LINE('',#7550,#1866);
#1527=LINE('',#7551,#1867);
#1528=LINE('',#7554,#1868);
#1529=LINE('',#7556,#1869);
#1530=LINE('',#7557,#1870);
#1531=LINE('',#7560,#1871);
#1532=LINE('',#7562,#1872);
#1533=LINE('',#7563,#1873);
#1534=LINE('',#7566,#1874);
#1535=LINE('',#7568,#1875);
#1536=LINE('',#7569,#1876);
#1537=LINE('',#7571,#1877);
#1538=LINE('',#7572,#1878);
#1855=VECTOR('',#6224,0.325);
#1856=VECTOR('',#6229,0.35);
#1857=VECTOR('',#6234,0.335);
#1858=VECTOR('',#6243,0.21);
#1859=VECTOR('',#6248,0.2);
#1860=VECTOR('',#6253,0.18);
#1861=VECTOR('',#6258,1.);
#1862=VECTOR('',#6259,1.);
#1863=VECTOR('',#6260,1.);
#1864=VECTOR('',#6261,1.);
#1865=VECTOR('',#6264,1.);
#1866=VECTOR('',#6265,1.);
#1867=VECTOR('',#6266,1.);
#1868=VECTOR('',#6269,1.);
#1869=VECTOR('',#6270,1.);
#1870=VECTOR('',#6271,1.);
#1871=VECTOR('',#6274,1.);
#1872=VECTOR('',#6275,1.);
#1873=VECTOR('',#6276,1.);
#1874=VECTOR('',#6279,1.);
#1875=VECTOR('',#6280,1.);
#1876=VECTOR('',#6281,1.);
#1877=VECTOR('',#6284,1.);
#1878=VECTOR('',#6285,1.);
#2090=CIRCLE('',#5037,0.3);
#2091=CIRCLE('',#5039,0.35);
#2092=CIRCLE('',#5041,0.35);
#2093=CIRCLE('',#5043,0.32);
#2094=CIRCLE('',#5045,0.22);
#2095=CIRCLE('',#5047,0.1954);
#2096=CIRCLE('',#5049,0.1954);
#2097=CIRCLE('',#5051,0.16);
#2401=VERTEX_POINT('',#7507);
#2402=VERTEX_POINT('',#7510);
#2403=VERTEX_POINT('',#7514);
#2404=VERTEX_POINT('',#7518);
#2405=VERTEX_POINT('',#7522);
#2406=VERTEX_POINT('',#7525);
#2407=VERTEX_POINT('',#7529);
#2408=VERTEX_POINT('',#7533);
#2409=VERTEX_POINT('',#7538);
#2410=VERTEX_POINT('',#7539);
#2411=VERTEX_POINT('',#7541);
#2412=VERTEX_POINT('',#7543);
#2413=VERTEX_POINT('',#7547);
#2414=VERTEX_POINT('',#7549);
#2415=VERTEX_POINT('',#7553);
#2416=VERTEX_POINT('',#7555);
#2417=VERTEX_POINT('',#7559);
#2418=VERTEX_POINT('',#7561);
#2419=VERTEX_POINT('',#7565);
#2420=VERTEX_POINT('',#7567);
#2892=EDGE_CURVE('',#2401,#2401,#2090,.T.);
#2893=EDGE_CURVE('',#2402,#2402,#2091,.T.);
#2894=EDGE_CURVE('',#2402,#2401,#1515,.T.);
#2895=EDGE_CURVE('',#2403,#2403,#2092,.T.);
#2896=EDGE_CURVE('',#2403,#2402,#1516,.T.);
#2897=EDGE_CURVE('',#2404,#2404,#2093,.T.);
#2898=EDGE_CURVE('',#2404,#2403,#1517,.T.);
#2899=EDGE_CURVE('',#2405,#2405,#2094,.T.);
#2900=EDGE_CURVE('',#2406,#2406,#2095,.F.);
#2901=EDGE_CURVE('',#2406,#2405,#1518,.T.);
#2902=EDGE_CURVE('',#2407,#2407,#2096,.F.);
#2903=EDGE_CURVE('',#2407,#2406,#1519,.T.);
#2904=EDGE_CURVE('',#2408,#2408,#2097,.T.);
#2905=EDGE_CURVE('',#2408,#2407,#1520,.T.);
#2906=EDGE_CURVE('',#2409,#2410,#1521,.T.);
#2907=EDGE_CURVE('',#2410,#2411,#1522,.T.);
#2908=EDGE_CURVE('',#2411,#2412,#1523,.T.);
#2909=EDGE_CURVE('',#2409,#2412,#1524,.T.);
#2910=EDGE_CURVE('',#2410,#2413,#1525,.T.);
#2911=EDGE_CURVE('',#2413,#2414,#1526,.T.);
#2912=EDGE_CURVE('',#2414,#2411,#1527,.T.);
#2913=EDGE_CURVE('',#2413,#2415,#1528,.T.);
#2914=EDGE_CURVE('',#2415,#2416,#1529,.T.);
#2915=EDGE_CURVE('',#2416,#2414,#1530,.T.);
#2916=EDGE_CURVE('',#2415,#2417,#1531,.T.);
#2917=EDGE_CURVE('',#2417,#2418,#1532,.T.);
#2918=EDGE_CURVE('',#2418,#2416,#1533,.T.);
#2919=EDGE_CURVE('',#2417,#2419,#1534,.T.);
#2920=EDGE_CURVE('',#2419,#2420,#1535,.T.);
#2921=EDGE_CURVE('',#2420,#2418,#1536,.T.);
#2922=EDGE_CURVE('',#2419,#2409,#1537,.T.);
#2923=EDGE_CURVE('',#2412,#2420,#1538,.T.);
#3848=ORIENTED_EDGE('',*,*,#2892,.F.);
#3849=ORIENTED_EDGE('',*,*,#2893,.F.);
#3850=ORIENTED_EDGE('',*,*,#2894,.T.);
#3851=ORIENTED_EDGE('',*,*,#2892,.T.);
#3852=ORIENTED_EDGE('',*,*,#2894,.F.);
#3853=ORIENTED_EDGE('',*,*,#2895,.F.);
#3854=ORIENTED_EDGE('',*,*,#2896,.T.);
#3855=ORIENTED_EDGE('',*,*,#2893,.T.);
#3856=ORIENTED_EDGE('',*,*,#2896,.F.);
#3857=ORIENTED_EDGE('',*,*,#2897,.F.);
#3858=ORIENTED_EDGE('',*,*,#2898,.T.);
#3859=ORIENTED_EDGE('',*,*,#2895,.T.);
#3860=ORIENTED_EDGE('',*,*,#2898,.F.);
#3861=ORIENTED_EDGE('',*,*,#2897,.T.);
#3862=ORIENTED_EDGE('',*,*,#2899,.F.);
#3863=ORIENTED_EDGE('',*,*,#2900,.F.);
#3864=ORIENTED_EDGE('',*,*,#2901,.T.);
#3865=ORIENTED_EDGE('',*,*,#2899,.T.);
#3866=ORIENTED_EDGE('',*,*,#2901,.F.);
#3867=ORIENTED_EDGE('',*,*,#2902,.F.);
#3868=ORIENTED_EDGE('',*,*,#2903,.T.);
#3869=ORIENTED_EDGE('',*,*,#2900,.T.);
#3870=ORIENTED_EDGE('',*,*,#2903,.F.);
#3871=ORIENTED_EDGE('',*,*,#2904,.F.);
#3872=ORIENTED_EDGE('',*,*,#2905,.T.);
#3873=ORIENTED_EDGE('',*,*,#2902,.T.);
#3874=ORIENTED_EDGE('',*,*,#2905,.F.);
#3875=ORIENTED_EDGE('',*,*,#2904,.T.);
#3876=ORIENTED_EDGE('',*,*,#2906,.T.);
#3877=ORIENTED_EDGE('',*,*,#2907,.T.);
#3878=ORIENTED_EDGE('',*,*,#2908,.T.);
#3879=ORIENTED_EDGE('',*,*,#2909,.F.);
#3880=ORIENTED_EDGE('',*,*,#2910,.T.);
#3881=ORIENTED_EDGE('',*,*,#2911,.T.);
#3882=ORIENTED_EDGE('',*,*,#2912,.T.);
#3883=ORIENTED_EDGE('',*,*,#2907,.F.);
#3884=ORIENTED_EDGE('',*,*,#2913,.T.);
#3885=ORIENTED_EDGE('',*,*,#2914,.T.);
#3886=ORIENTED_EDGE('',*,*,#2915,.T.);
#3887=ORIENTED_EDGE('',*,*,#2911,.F.);
#3888=ORIENTED_EDGE('',*,*,#2916,.T.);
#3889=ORIENTED_EDGE('',*,*,#2917,.T.);
#3890=ORIENTED_EDGE('',*,*,#2918,.T.);
#3891=ORIENTED_EDGE('',*,*,#2914,.F.);
#3892=ORIENTED_EDGE('',*,*,#2919,.T.);
#3893=ORIENTED_EDGE('',*,*,#2920,.T.);
#3894=ORIENTED_EDGE('',*,*,#2921,.T.);
#3895=ORIENTED_EDGE('',*,*,#2917,.F.);
#3896=ORIENTED_EDGE('',*,*,#2922,.T.);
#3897=ORIENTED_EDGE('',*,*,#2909,.T.);
#3898=ORIENTED_EDGE('',*,*,#2923,.T.);
#3899=ORIENTED_EDGE('',*,*,#2920,.F.);
#3900=ORIENTED_EDGE('',*,*,#2922,.F.);
#3901=ORIENTED_EDGE('',*,*,#2919,.F.);
#3902=ORIENTED_EDGE('',*,*,#2916,.F.);
#3903=ORIENTED_EDGE('',*,*,#2913,.F.);
#3904=ORIENTED_EDGE('',*,*,#2910,.F.);
#3905=ORIENTED_EDGE('',*,*,#2906,.F.);
#3906=ORIENTED_EDGE('',*,*,#2923,.F.);
#3907=ORIENTED_EDGE('',*,*,#2908,.F.);
#3908=ORIENTED_EDGE('',*,*,#2912,.F.);
#3909=ORIENTED_EDGE('',*,*,#2915,.F.);
#3910=ORIENTED_EDGE('',*,*,#2918,.F.);
#3911=ORIENTED_EDGE('',*,*,#2921,.F.);
#4127=CYLINDRICAL_SURFACE('',#5040,0.35);
#4128=CYLINDRICAL_SURFACE('',#5048,0.1954);
#4337=ADVANCED_FACE('',(#818),#581,.T.);
#4338=ADVANCED_FACE('',(#819),#248,.T.);
#4339=ADVANCED_FACE('',(#820),#4127,.T.);
#4340=ADVANCED_FACE('',(#821),#249,.T.);
#4341=ADVANCED_FACE('',(#822,#454),#582,.T.);
#4342=ADVANCED_FACE('',(#823),#250,.T.);
#4343=ADVANCED_FACE('',(#824),#4128,.T.);
#4344=ADVANCED_FACE('',(#825),#251,.T.);
#4345=ADVANCED_FACE('',(#826),#583,.T.);
#4346=ADVANCED_FACE('',(#827),#584,.F.);
#4347=ADVANCED_FACE('',(#828),#585,.F.);
#4348=ADVANCED_FACE('',(#829),#586,.F.);
#4349=ADVANCED_FACE('',(#830),#587,.F.);
#4350=ADVANCED_FACE('',(#831),#588,.F.);
#4351=ADVANCED_FACE('',(#832),#589,.F.);
#4352=ADVANCED_FACE('',(#833),#590,.F.);
#4353=ADVANCED_FACE('',(#834),#591,.F.);
#4410=CLOSED_SHELL('',(#4337,#4338,#4339,#4340,#4341,#4342,#4343,#4344,
#4345));
#4411=CLOSED_SHELL('',(#4346,#4347,#4348,#4349,#4350,#4351,#4352,#4353));
#5035=AXIS2_PLACEMENT_3D('',#7505,#6214,#6215);
#5036=AXIS2_PLACEMENT_3D('',#7506,#6216,#6217);
#5037=AXIS2_PLACEMENT_3D('',#7508,#6218,#6219);
#5038=AXIS2_PLACEMENT_3D('',#7509,#6220,#6221);
#5039=AXIS2_PLACEMENT_3D('',#7511,#6222,#6223);
#5040=AXIS2_PLACEMENT_3D('',#7513,#6225,#6226);
#5041=AXIS2_PLACEMENT_3D('',#7515,#6227,#6228);
#5042=AXIS2_PLACEMENT_3D('',#7517,#6230,#6231);
#5043=AXIS2_PLACEMENT_3D('',#7519,#6232,#6233);
#5044=AXIS2_PLACEMENT_3D('',#7521,#6235,#6236);
#5045=AXIS2_PLACEMENT_3D('',#7523,#6237,#6238);
#5046=AXIS2_PLACEMENT_3D('',#7524,#6239,#6240);
#5047=AXIS2_PLACEMENT_3D('',#7526,#6241,#6242);
#5048=AXIS2_PLACEMENT_3D('',#7528,#6244,#6245);
#5049=AXIS2_PLACEMENT_3D('',#7530,#6246,#6247);
#5050=AXIS2_PLACEMENT_3D('',#7532,#6249,#6250);
#5051=AXIS2_PLACEMENT_3D('',#7534,#6251,#6252);
#5052=AXIS2_PLACEMENT_3D('',#7536,#6254,#6255);
#5053=AXIS2_PLACEMENT_3D('',#7537,#6256,#6257);
#5054=AXIS2_PLACEMENT_3D('',#7546,#6262,#6263);
#5055=AXIS2_PLACEMENT_3D('',#7552,#6267,#6268);
#5056=AXIS2_PLACEMENT_3D('',#7558,#6272,#6273);
#5057=AXIS2_PLACEMENT_3D('',#7564,#6277,#6278);
#5058=AXIS2_PLACEMENT_3D('',#7570,#6282,#6283);
#5059=AXIS2_PLACEMENT_3D('',#7573,#6286,#6287);
#5060=AXIS2_PLACEMENT_3D('',#7574,#6288,#6289);
#6214=DIRECTION('axis',(0.,0.,1.));
#6215=DIRECTION('refdir',(1.,0.,0.));
#6216=DIRECTION('center_axis',(0.,1.,0.));
#6217=DIRECTION('ref_axis',(0.,0.,1.));
#6218=DIRECTION('center_axis',(0.,-1.,0.));
#6219=DIRECTION('ref_axis',(1.,0.,0.));
#6220=DIRECTION('center_axis',(0.,-1.,0.));
#6221=DIRECTION('ref_axis',(1.,0.,0.));
#6222=DIRECTION('center_axis',(0.,-1.,0.));
#6223=DIRECTION('ref_axis',(1.,0.,0.));
#6224=DIRECTION('',(0.707106781186547,0.707106781186548,8.65956056235493E-17));
#6225=DIRECTION('center_axis',(0.,-1.,0.));
#6226=DIRECTION('ref_axis',(1.,0.,0.));
#6227=DIRECTION('center_axis',(0.,-1.,0.));
#6228=DIRECTION('ref_axis',(1.,0.,0.));
#6229=DIRECTION('',(0.,1.,0.));
#6230=DIRECTION('center_axis',(0.,1.,0.));
#6231=DIRECTION('ref_axis',(1.,0.,0.));
#6232=DIRECTION('center_axis',(0.,-1.,0.));
#6233=DIRECTION('ref_axis',(1.,0.,0.));
#6234=DIRECTION('',(-0.707106781186547,0.707106781186548,-8.65956056235493E-17));
#6235=DIRECTION('center_axis',(0.,-1.,0.));
#6236=DIRECTION('ref_axis',(0.,0.,-1.));
#6237=DIRECTION('center_axis',(0.,-1.,0.));
#6238=DIRECTION('ref_axis',(1.,0.,0.));
#6239=DIRECTION('center_axis',(0.,1.,0.));
#6240=DIRECTION('ref_axis',(1.,0.,0.));
#6241=DIRECTION('center_axis',(0.,1.,0.));
#6242=DIRECTION('ref_axis',(1.,0.,0.));
#6243=DIRECTION('',(-0.447213595499958,0.894427190999916,-5.47678698264203E-17));
#6244=DIRECTION('center_axis',(0.,-1.,0.));
#6245=DIRECTION('ref_axis',(1.,0.,0.));
#6246=DIRECTION('center_axis',(0.,1.,0.));
#6247=DIRECTION('ref_axis',(1.,0.,0.));
#6248=DIRECTION('',(0.,1.,0.));
#6249=DIRECTION('center_axis',(0.,1.,0.));
#6250=DIRECTION('ref_axis',(1.,0.,0.));
#6251=DIRECTION('center_axis',(0.,-1.,0.));
#6252=DIRECTION('ref_axis',(1.,0.,0.));
#6253=DIRECTION('',(-0.707106781186547,0.707106781186548,-8.65956056235493E-17));
#6254=DIRECTION('center_axis',(0.,-1.,0.));
#6255=DIRECTION('ref_axis',(0.,0.,-1.));
#6256=DIRECTION('center_axis',(0.866025403784439,0.,-0.5));
#6257=DIRECTION('ref_axis',(0.5,0.,0.866025403784439));
#6258=DIRECTION('',(-0.5,0.,-0.866025403784439));
#6259=DIRECTION('',(0.,-1.,0.));
#6260=DIRECTION('',(0.5,0.,0.866025403784439));
#6261=DIRECTION('',(0.,-1.,0.));
#6262=DIRECTION('center_axis',(1.60246890531964E-16,0.,-1.));
#6263=DIRECTION('ref_axis',(1.,0.,1.60246890531964E-16));
#6264=DIRECTION('',(-1.,0.,-1.60246890531964E-16));
#6265=DIRECTION('',(0.,-1.,0.));
#6266=DIRECTION('',(1.,0.,1.60246890531964E-16));
#6267=DIRECTION('center_axis',(-0.866025403784439,0.,-0.5));
#6268=DIRECTION('ref_axis',(0.5,0.,-0.866025403784439));
#6269=DIRECTION('',(-0.5,0.,0.866025403784439));
#6270=DIRECTION('',(0.,-1.,0.));
#6271=DIRECTION('',(0.5,0.,-0.866025403784439));
#6272=DIRECTION('center_axis',(-0.866025403784439,0.,0.5));
#6273=DIRECTION('ref_axis',(-0.5,0.,-0.866025403784439));
#6274=DIRECTION('',(0.5,0.,0.866025403784439));
#6275=DIRECTION('',(0.,-1.,0.));
#6276=DIRECTION('',(-0.5,0.,-0.866025403784439));
#6277=DIRECTION('center_axis',(-1.60246890531964E-16,0.,1.));
#6278=DIRECTION('ref_axis',(-1.,0.,-1.60246890531964E-16));
#6279=DIRECTION('',(1.,0.,1.60246890531964E-16));
#6280=DIRECTION('',(0.,-1.,0.));
#6281=DIRECTION('',(-1.,0.,-1.60246890531964E-16));
#6282=DIRECTION('center_axis',(0.866025403784439,0.,0.5));
#6283=DIRECTION('ref_axis',(-0.5,0.,0.866025403784439));
#6284=DIRECTION('',(0.5,0.,-0.866025403784439));
#6285=DIRECTION('',(-0.5,0.,0.866025403784439));
#6286=DIRECTION('center_axis',(0.,1.,0.));
#6287=DIRECTION('ref_axis',(1.,0.,0.));
#6288=DIRECTION('center_axis',(0.,-1.,0.));
#6289=DIRECTION('ref_axis',(0.,0.,-1.));
#7505=CARTESIAN_POINT('',(0.,0.,0.));
#7506=CARTESIAN_POINT('Origin',(0.3,0.4,0.));
#7507=CARTESIAN_POINT('',(-0.3,0.4,-3.67394039744206E-17));
#7508=CARTESIAN_POINT('Origin',(0.,0.4,0.));
#7509=CARTESIAN_POINT('Origin',(0.,0.375,0.));
#7510=CARTESIAN_POINT('',(-0.35,0.35,-4.28626379701573E-17));
#7511=CARTESIAN_POINT('Origin',(0.,0.35,0.));
#7512=CARTESIAN_POINT('',(-0.325,0.375,-3.9801020972289E-17));
#7513=CARTESIAN_POINT('Origin',(0.,0.19,0.));
#7514=CARTESIAN_POINT('',(-0.35,0.03,-4.28626379701574E-17));
#7515=CARTESIAN_POINT('Origin',(0.,0.03,0.));
#7516=CARTESIAN_POINT('',(-0.35,0.19,-4.28626379701574E-17));
#7517=CARTESIAN_POINT('Origin',(0.,0.0149999999999999,0.));
#7518=CARTESIAN_POINT('',(-0.32,-3.29597460435593E-17,-3.91886975727153E-17));
#7519=CARTESIAN_POINT('Origin',(0.,0.,0.));
#7520=CARTESIAN_POINT('',(-0.335,0.0149999999999999,-4.10256677714363E-17));
#7521=CARTESIAN_POINT('Origin',(0.22,0.,0.));
#7522=CARTESIAN_POINT('',(-0.22,-6.93889390390723E-18,-2.69422295812418E-17));
#7523=CARTESIAN_POINT('Origin',(0.,0.,0.));
#7524=CARTESIAN_POINT('Origin',(0.,-0.02,0.));
#7525=CARTESIAN_POINT('',(-0.1954,-0.0492,2.39295984553393E-17));
#7526=CARTESIAN_POINT('Origin',(0.,-0.0492,0.));
#7527=CARTESIAN_POINT('',(-0.21,-0.02,-2.57175827820944E-17));
#7528=CARTESIAN_POINT('Origin',(0.,-0.8,0.));
#7529=CARTESIAN_POINT('',(-0.1954,-1.5646,2.39295984553393E-17));
#7530=CARTESIAN_POINT('Origin',(0.,-1.5646,0.));
#7531=CARTESIAN_POINT('',(-0.1954,-0.8,-2.39295984553393E-17));
#7532=CARTESIAN_POINT('Origin',(0.,-1.58,0.));
#7533=CARTESIAN_POINT('',(-0.16,-1.6,-1.95943487863577E-17));
#7534=CARTESIAN_POINT('Origin',(0.,-1.6,0.));
#7535=CARTESIAN_POINT('',(-0.18,-1.58,-2.20436423846524E-17));
#7536=CARTESIAN_POINT('Origin',(0.,-1.6,0.));
#7537=CARTESIAN_POINT('Origin',(0.0866025403784439,-0.4,-0.15));
#7538=CARTESIAN_POINT('',(0.173205080756888,-0.4,0.));
#7539=CARTESIAN_POINT('',(0.0866025403784439,-0.4,-0.15));
#7540=CARTESIAN_POINT('',(0.173205080756888,-0.4,0.));
#7541=CARTESIAN_POINT('',(0.0866025403784439,-0.64,-0.15));
#7542=CARTESIAN_POINT('',(0.0866025403784439,-0.4,-0.15));
#7543=CARTESIAN_POINT('',(0.173205080756888,-0.64,0.));
#7544=CARTESIAN_POINT('',(0.173205080756888,-0.64,0.));
#7545=CARTESIAN_POINT('',(0.173205080756888,-0.4,0.));
#7546=CARTESIAN_POINT('Origin',(-0.0866025403784438,-0.4,-0.15));
#7547=CARTESIAN_POINT('',(-0.0866025403784438,-0.4,-0.15));
#7548=CARTESIAN_POINT('',(0.0866025403784439,-0.4,-0.15));
#7549=CARTESIAN_POINT('',(-0.0866025403784438,-0.64,-0.15));
#7550=CARTESIAN_POINT('',(-0.0866025403784438,-0.4,-0.15));
#7551=CARTESIAN_POINT('',(0.0866025403784439,-0.64,-0.15));
#7552=CARTESIAN_POINT('Origin',(-0.173205080756888,-0.4,-2.77555756156289E-17));
#7553=CARTESIAN_POINT('',(-0.173205080756888,-0.4,-2.12115047744981E-17));
#7554=CARTESIAN_POINT('',(-0.0866025403784438,-0.4,-0.15));
#7555=CARTESIAN_POINT('',(-0.173205080756888,-0.64,-2.77555756156289E-17));
#7556=CARTESIAN_POINT('',(-0.173205080756888,-0.4,-2.12115047744981E-17));
#7557=CARTESIAN_POINT('',(-0.0866025403784438,-0.64,-0.15));
#7558=CARTESIAN_POINT('Origin',(-0.0866025403784439,-0.4,0.15));
#7559=CARTESIAN_POINT('',(-0.0866025403784439,-0.4,0.15));
#7560=CARTESIAN_POINT('',(-0.173205080756888,-0.4,-2.12115047744981E-17));
#7561=CARTESIAN_POINT('',(-0.0866025403784439,-0.64,0.15));
#7562=CARTESIAN_POINT('',(-0.0866025403784439,-0.4,0.15));
#7563=CARTESIAN_POINT('',(-0.173205080756888,-0.64,-2.12115047744981E-17));
#7564=CARTESIAN_POINT('Origin',(0.0866025403784439,-0.4,0.15));
#7565=CARTESIAN_POINT('',(0.0866025403784439,-0.4,0.15));
#7566=CARTESIAN_POINT('',(-0.0866025403784439,-0.4,0.15));
#7567=CARTESIAN_POINT('',(0.0866025403784439,-0.64,0.15));
#7568=CARTESIAN_POINT('',(0.0866025403784439,-0.4,0.15));
#7569=CARTESIAN_POINT('',(-0.0866025403784439,-0.64,0.15));
#7570=CARTESIAN_POINT('Origin',(0.173205080756888,-0.4,0.));
#7571=CARTESIAN_POINT('',(0.0866025403784439,-0.4,0.15));
#7572=CARTESIAN_POINT('',(0.0866025403784439,-0.64,0.15));
#7573=CARTESIAN_POINT('Origin',(0.,-0.4,-2.77555756156289E-17));
#7574=CARTESIAN_POINT('Origin',(0.,-0.64,-2.77555756156289E-17));
#7805=UNCERTAINTY_MEASURE_WITH_UNIT(LENGTH_MEASURE(0.001),#7836,
'DISTANCE_ACCURACY_VALUE',
'Maximum model space distance between geometric entities at asserted c
onnectivities');
#7809=UNCERTAINTY_MEASURE_WITH_UNIT(LENGTH_MEASURE(0.001),#7836,
'DISTANCE_ACCURACY_VALUE',
'Maximum model space distance between geometric entities at asserted c
onnectivities');
#7831=(
GEOMETRIC_REPRESENTATION_CONTEXT(3)
GLOBAL_UNCERTAINTY_ASSIGNED_CONTEXT((#7805))
GLOBAL_UNIT_ASSIGNED_CONTEXT((#7836,#7838,#7839))
REPRESENTATION_CONTEXT('','3D')
);
#7835=(
GEOMETRIC_REPRESENTATION_CONTEXT(3)
GLOBAL_UNCERTAINTY_ASSIGNED_CONTEXT((#7809))
GLOBAL_UNIT_ASSIGNED_CONTEXT((#7836,#7838,#7839))
REPRESENTATION_CONTEXT('','3D')
);
#7836=(
LENGTH_UNIT()
NAMED_UNIT(*)
SI_UNIT(.CENTI.,.METRE.)
);
#7838=(
NAMED_UNIT(*)
PLANE_ANGLE_UNIT()
SI_UNIT($,.RADIAN.)
);
#7839=(
NAMED_UNIT(*)
SI_UNIT($,.STERADIAN.)
SOLID_ANGLE_UNIT()
);
#7861=SHAPE_DEFINITION_REPRESENTATION(#7888,#7967);
#7888=PRODUCT_DEFINITION_SHAPE('',$,#7993);
#7967=SHAPE_REPRESENTATION('',(#5035),#7831);
#7971=PRODUCT_DEFINITION_CONTEXT('part definition',#8048,'design');
#7993=PRODUCT_DEFINITION('Cap Screw - M4x16','Cap Screw - M4x16',#8018,
#7971);
#8018=PRODUCT_DEFINITION_FORMATION('',$,#8071);
#8048=APPLICATION_CONTEXT(
'Core Data for Automotive Mechanical Design Process');
#8049=PRODUCT_CONTEXT('part definition',#8048,'mechanical');
#8071=PRODUCT('Cap Screw - M4x16','Cap Screw - M4x16',
'Cap Screw - M4x16',(#8049));
#8145=COLOUR_RGB('Black',0.12,0.14,0.17);
#8146=FILL_AREA_STYLE_COLOUR('',#8145);
#8147=FILL_AREA_STYLE('',(#8146));
#8148=SURFACE_STYLE_FILL_AREA(#8147);
#8149=SURFACE_SIDE_STYLE('',(#8148));
#8150=SURFACE_STYLE_USAGE(.BOTH.,#8149);
#8151=PRESENTATION_STYLE_ASSIGNMENT((#8150));
ENDSEC;
END-ISO-10303-21;
